ISO-10303-21;
HEADER;
FILE_DESCRIPTION((''),'2;1');
FILE_NAME('MOUNTING_SCREW_M3x8.step','2026-10-01T22:07:29-07:00',(''),(''),'','','');
FILE_SCHEMA (('AUTOMOTIVE_DESIGN { 1 0 10303 214 3 1 1 }'));
ENDSEC;
DATA;
#10=MECHANICAL_DESIGN_GEOMETRIC_PRESENTATION_REPRESENTATION('',(#584),#15484);
#507=SHAPE_REPRESENTATION_RELATIONSHIP('SRR','None',#15659,#542) ;
#542=ADVANCED_BREP_SHAPE_REPRESENTATION('',(#625),#15483) ;
#584=STYLED_ITEM('',(#15832),#625) ;
#625=MANIFOLD_SOLID_BREP('MOUNTING_SCREW_M3x8',#8295) ;
#808=CYLINDRICAL_SURFACE('',#9906,0.15) ;
#809=CYLINDRICAL_SURFACE('',#9910,0.275) ;
#884=FACE_BOUND('',#2439,.T.) ;
#1361=CIRCLE('',#9907,0.15) ;
#1362=CIRCLE('',#9908,0.15) ;
#1363=CIRCLE('',#9911,0.275) ;
#1364=CIRCLE('',#9912,0.275) ;
#1860=FACE_OUTER_BOUND('',#2434,.T.) ;
#1861=FACE_OUTER_BOUND('',#2435,.T.) ;
#1862=FACE_OUTER_BOUND('',#2436,.T.) ;
#1863=FACE_OUTER_BOUND('',#2437,.T.) ;
#1864=FACE_OUTER_BOUND('',#2438,.T.) ;
#2434=EDGE_LOOP('',(#7525,#7526,#7527,#7528)) ;
#2435=EDGE_LOOP('',(#7529)) ;
#2436=EDGE_LOOP('',(#7530,#7531,#7532,#7533)) ;
#2437=EDGE_LOOP('',(#7534)) ;
#2438=EDGE_LOOP('',(#7535)) ;
#2439=EDGE_LOOP('',(#7536)) ;
#2912=LINE('',#15378,#3386) ;
#2913=LINE('',#15385,#3387) ;
#3386=VECTOR('',#12849,0.15) ;
#3387=VECTOR('',#12858,0.275) ;
#4137=VERTEX_POINT('',#15375) ;
#4138=VERTEX_POINT('',#15377) ;
#4139=VERTEX_POINT('',#15382) ;
#4140=VERTEX_POINT('',#15384) ;
#5267=EDGE_CURVE('',#4137,#4137,#1361,.T.) ;
#5268=EDGE_CURVE('',#4137,#4138,#2912,.T.) ;
#5269=EDGE_CURVE('',#4138,#4138,#1362,.T.) ;
#5270=EDGE_CURVE('',#4139,#4139,#1363,.T.) ;
#5271=EDGE_CURVE('',#4139,#4140,#2913,.T.) ;
#5272=EDGE_CURVE('',#4140,#4140,#1364,.T.) ;
#7525=ORIENTED_EDGE('',*,*,#5267,.F.) ;
#7526=ORIENTED_EDGE('',*,*,#5268,.T.) ;
#7527=ORIENTED_EDGE('',*,*,#5269,.F.) ;
#7528=ORIENTED_EDGE('',*,*,#5268,.F.) ;
#7529=ORIENTED_EDGE('',*,*,#5267,.T.) ;
#7530=ORIENTED_EDGE('',*,*,#5270,.F.) ;
#7531=ORIENTED_EDGE('',*,*,#5271,.T.) ;
#7532=ORIENTED_EDGE('',*,*,#5272,.F.) ;
#7533=ORIENTED_EDGE('',*,*,#5271,.F.) ;
#7534=ORIENTED_EDGE('',*,*,#5272,.T.) ;
#7535=ORIENTED_EDGE('',*,*,#5270,.T.) ;
#7536=ORIENTED_EDGE('',*,*,#5269,.T.) ;
#7749=PLANE('',#9909) ;
#7750=PLANE('',#9913) ;
#7751=PLANE('',#9914) ;
#8247=ADVANCED_FACE('',(#1860),#808,.T.) ;
#8248=ADVANCED_FACE('',(#1861),#7749,.T.) ;
#8249=ADVANCED_FACE('',(#1862),#809,.T.) ;
#8250=ADVANCED_FACE('',(#1863),#7750,.T.) ;
#8251=ADVANCED_FACE('',(#1864,#884),#7751,.T.) ;
#8295=CLOSED_SHELL('',(#8247,#8248,#8249,#8250,#8251)) ;
#9905=AXIS2_PLACEMENT_3D('',#15373,#12843,#12844) ;
#9906=AXIS2_PLACEMENT_3D('',#15374,#12845,#12846) ;
#9907=AXIS2_PLACEMENT_3D('',#15376,#12847,#12848) ;
#9908=AXIS2_PLACEMENT_3D('',#15379,#12850,#12851) ;
#9909=AXIS2_PLACEMENT_3D('',#15380,#12852,#12853) ;
#9910=AXIS2_PLACEMENT_3D('',#15381,#12854,#12855) ;
#9911=AXIS2_PLACEMENT_3D('',#15383,#12856,#12857) ;
#9912=AXIS2_PLACEMENT_3D('',#15386,#12859,#12860) ;
#9913=AXIS2_PLACEMENT_3D('',#15387,#12861,#12862) ;
#9914=AXIS2_PLACEMENT_3D('',#15388,#12863,#12864) ;
#12843=DIRECTION('axis',(0.,0.,1.)) ;
#12844=DIRECTION('refdir',(1.,0.,0.)) ;
#12845=DIRECTION('center_axis',(0.,0.,1.)) ;
#12846=DIRECTION('ref_axis',(1.,0.,0.)) ;
#12847=DIRECTION('center_axis',(0.,0.,1.)) ;
#12848=DIRECTION('ref_axis',(1.,0.,0.)) ;
#12849=DIRECTION('',(0.,0.,-1.)) ;
#12850=DIRECTION('center_axis',(0.,0.,-1.)) ;
#12851=DIRECTION('ref_axis',(1.,0.,0.)) ;
#12852=DIRECTION('center_axis',(0.,0.,1.)) ;
#12853=DIRECTION('ref_axis',(1.,0.,0.)) ;
#12854=DIRECTION('center_axis',(0.,0.,1.)) ;
#12855=DIRECTION('ref_axis',(1.,0.,0.)) ;
#12856=DIRECTION('center_axis',(0.,0.,1.)) ;
#12857=DIRECTION('ref_axis',(1.,0.,0.)) ;
#12858=DIRECTION('',(0.,0.,-1.)) ;
#12859=DIRECTION('center_axis',(0.,0.,-1.)) ;
#12860=DIRECTION('ref_axis',(1.,0.,0.)) ;
#12861=DIRECTION('center_axis',(0.,0.,-1.)) ;
#12862=DIRECTION('ref_axis',(-1.,0.,0.)) ;
#12863=DIRECTION('center_axis',(0.,0.,1.)) ;
#12864=DIRECTION('ref_axis',(1.,0.,0.)) ;
#15373=CARTESIAN_POINT('',(0.,0.,0.)) ;
#15374=CARTESIAN_POINT('Origin',(0.,0.,0.4)) ;
#15375=CARTESIAN_POINT('',(-0.15,-1.83697019872103E-17,0.8)) ;
#15376=CARTESIAN_POINT('Origin',(0.,0.,0.8)) ;
#15377=CARTESIAN_POINT('',(-0.15,-1.83697019872103E-17,0.)) ;
#15378=CARTESIAN_POINT('',(-0.15,-1.83697019872103E-17,0.4)) ;
#15379=CARTESIAN_POINT('Origin',(0.,0.,0.)) ;
#15380=CARTESIAN_POINT('Origin',(0.,0.,0.8)) ;
#15381=CARTESIAN_POINT('Origin',(0.,0.,-0.1)) ;
#15382=CARTESIAN_POINT('',(-0.275,-3.36777869765522E-17,0.)) ;
#15383=CARTESIAN_POINT('Origin',(0.,0.,0.)) ;
#15384=CARTESIAN_POINT('',(-0.275,-3.36777869765522E-17,-0.2)) ;
#15385=CARTESIAN_POINT('',(-0.275,-3.36777869765522E-17,-0.1)) ;
#15386=CARTESIAN_POINT('Origin',(0.,0.,-0.2)) ;
#15387=CARTESIAN_POINT('Origin',(0.,0.,-0.2)) ;
#15388=CARTESIAN_POINT('Origin',(0.,0.,0.)) ;
#15440=UNCERTAINTY_MEASURE_WITH_UNIT(LENGTH_MEASURE(0.001),#15485,
'DISTANCE_ACCURACY_VALUE',
'Maximum model space distance between geometric entities at asserted c
onnectivities') ;
#15441=UNCERTAINTY_MEASURE_WITH_UNIT(LENGTH_MEASURE(0.001),#15485,
'DISTANCE_ACCURACY_VALUE',
'Maximum model space distance between geometric entities at asserted c
onnectivities') ;
#15483=(
GEOMETRIC_REPRESENTATION_CONTEXT(3)
GLOBAL_UNCERTAINTY_ASSIGNED_CONTEXT((#15440))
GLOBAL_UNIT_ASSIGNED_CONTEXT((#15485,#15487,#15488))
REPRESENTATION_CONTEXT('','3D')
) ;
#15484=(
GEOMETRIC_REPRESENTATION_CONTEXT(3)
GLOBAL_UNCERTAINTY_ASSIGNED_CONTEXT((#15441))
GLOBAL_UNIT_ASSIGNED_CONTEXT((#15485,#15487,#15488))
REPRESENTATION_CONTEXT('','3D')
) ;
#15485=(
LENGTH_UNIT()
NAMED_UNIT(*)
SI_UNIT(.CENTI.,.METRE.)
) ;
#15487=(
NAMED_UNIT(*)
PLANE_ANGLE_UNIT()
SI_UNIT($,.RADIAN.)
) ;
#15488=(
NAMED_UNIT(*)
SI_UNIT($,.STERADIAN.)
SOLID_ANGLE_UNIT()
) ;
#15530=SHAPE_DEFINITION_REPRESENTATION(#15607,#15659) ;
#15607=PRODUCT_DEFINITION_SHAPE('',$,#15702) ;
#15659=SHAPE_REPRESENTATION('',(#9905),#15483) ;
#15660=PRODUCT_DEFINITION_CONTEXT('part definition',#15788,'design') ;
#15702=PRODUCT_DEFINITION('MOUNTING_SCREW_M3x8',
'MOUNTING_SCREW_M3x8',#15744,#15660) ;
#15744=PRODUCT_DEFINITION_FORMATION('',$,#15831) ;
#15788=APPLICATION_CONTEXT(
'Core Data for Automotive Mechanical Design Process') ;
#15789=PRODUCT_CONTEXT('part definition',#15788,'mechanical') ;
#15831=PRODUCT('MOUNTING_SCREW_M3x8','MOUNTING_SCREW_M3x8',$,(#15789)) ;
#15832=PRESENTATION_STYLE_ASSIGNMENT((#15844)) ;
#15844=SURFACE_STYLE_USAGE(.BOTH.,#15856) ;
#15856=SURFACE_SIDE_STYLE('',(#15868)) ;
#15868=SURFACE_STYLE_FILL_AREA(#15880) ;
#15880=FILL_AREA_STYLE('Steel - Satin',(#15892)) ;
#15892=FILL_AREA_STYLE_COLOUR('Steel - Satin',#15904) ;
#15904=COLOUR_RGB('Steel - Satin', 0.72549020, 0.75294118, 0.79215686) ;
ENDSEC;
END-ISO-10303-21;
